ISO-10303-21;
HEADER;
FILE_DESCRIPTION (('STEP AP214'),
    '1' );
FILE_NAME ('Ball Valve Sub.step',
    '2026-10-23T18:01:19',
    ( '' ),
    ( '' ),
    'SwSTEP 2.0',
    'SolidWorks 2025',
    '' );
FILE_SCHEMA (( 'AUTOMOTIVE_DESIGN' ));
ENDSEC;

DATA;
#73=DIRECTION ( 'NONE',  ( 0.000000000000000000, 0.000000000000000000, 1.000000000000000000 ) ) ;
#81=DIRECTION ( 'NONE',  ( 0.000000000000000000, 0.000000000000000000, -1.000000000000000000 ) ) ;
#95=CARTESIAN_POINT ( 'NONE',  ( 0.000000000000000000, 4.529999999999999361, 0.000000000000000000 ) ) ;
#98=ORIENTED_EDGE ( 'NONE', *, *, #14017, .F. ) ;
#134=ORIENTED_EDGE ( 'NONE', *, *, #1959, .F. ) ;
#138=CARTESIAN_POINT ( 'NONE',  ( 0.2849999999999996425, 0.000000000000000000, 0.4108223460329292753 ) ) ;
#145=CARTESIAN_POINT ( 'NONE',  ( 6.123233995736763571E-17, 4.529999999999999361, 0.4999999999999997224 ) ) ;
#200=DIRECTION ( 'NONE',  ( -1.000000000000000000, 0.000000000000000000, -1.047444401652940007E-14 ) ) ;
#250=DIRECTION ( 'NONE',  ( 0.000000000000000000, 1.000000000000000000, -0.000000000000000000 ) ) ;
#256=CIRCLE ( 'NONE', #12476, 0.4999999999999995004 ) ;
#315=CARTESIAN_POINT ( 'NONE',  ( 0.4108223460329304411, 5.750000000000000000, -0.2849999999999985323 ) ) ;
#325=ADVANCED_FACE ( 'NONE', ( #5492 ), #796, .F. ) ;
#395=CARTESIAN_POINT ( 'NONE',  ( 0.000000000000000000, 1.000000000000000000, 0.000000000000000000 ) ) ;
#454=ADVANCED_FACE ( 'NONE', ( #14039 ), #12817, .T. ) ;
#510=CIRCLE ( 'NONE', #6642, 1.000000000000000000 ) ;
#564=DIRECTION ( 'NONE',  ( -0.000000000000000000, -0.000000000000000000, 1.000000000000000000 ) ) ;
#610=DIRECTION ( 'NONE',  ( -0.000000000000000000, -1.000000000000000000, -0.000000000000000000 ) ) ;
#639=CARTESIAN_POINT ( 'NONE',  ( 0.2849999999999999201, 0.000000000000000000, -0.4108223460329290533 ) ) ;
#640=LINE ( 'NONE', #3962, #6834 ) ;
#644=CARTESIAN_POINT ( 'NONE',  ( 0.000000000000000000, 1.000000000000000000, -1.000000000000000000 ) ) ;
#658=LENGTH_MEASURE_WITH_UNIT ( LENGTH_MEASURE( 0.02539999999999999897 ), #4132 );
#719=CARTESIAN_POINT ( 'NONE',  ( 0.4108223460329280541, 0.000000000000000000, 0.2850000000000013078 ) ) ;
#735=( NAMED_UNIT ( * ) SI_UNIT ( $, .STERADIAN. ) SOLID_ANGLE_UNIT ( ) );
#782=ADVANCED_FACE ( 'NONE', ( #13010 ), #2472, .F. ) ;
#796=CYLINDRICAL_SURFACE ( 'NONE', #10578, 0.7500000000000001110 ) ;
#807=( NAMED_UNIT ( * ) PLANE_ANGLE_UNIT ( ) SI_UNIT ( $, .RADIAN. ) );
#846=ORIENTED_EDGE ( 'NONE', *, *, #5437, .T. ) ;
#852=CIRCLE ( 'NONE', #6252, 0.4999999999999995004 ) ;
#858=ORIENTED_EDGE ( 'NONE', *, *, #6303, .T. ) ;
#861=CIRCLE ( 'NONE', #4805, 0.4999999999999997224 ) ;
#864=CARTESIAN_POINT ( 'NONE',  ( 0.4108223460329283871, 5.750000000000000000, 0.2850000000000014189 ) ) ;
#885=EDGE_CURVE ( 'NONE', #1422, #2642, #6660, .T. ) ;
#904=DIRECTION ( 'NONE',  ( -1.000000000000000000, 0.000000000000000000, -1.047444401652940007E-14 ) ) ;
#909=VERTEX_POINT ( 'NONE', #13161 ) ;
#938=CARTESIAN_POINT ( 'NONE',  ( -0.4108223460329323840, 4.529999999999999361, 0.2849999999999956457 ) ) ;
#957=CARTESIAN_POINT ( 'NONE',  ( 0.000000000000000000, 0.000000000000000000, 0.000000000000000000 ) ) ;
#970=DIRECTION ( 'NONE',  ( -0.000000000000000000, -1.000000000000000000, -0.000000000000000000 ) ) ;
#997=EDGE_LOOP ( 'NONE', ( #8693, #7422, #5563, #6768 ) ) ;
#1031=LINE ( 'NONE', #4884, #2952 ) ;
#1036=EDGE_LOOP ( 'NONE', ( #10242, #8055, #6195, #14488, #8462, #4157, #8619, #12945 ) ) ;
#1059=CARTESIAN_POINT ( 'NONE',  ( 0.000000000000000000, 4.529999999999999361, 0.000000000000000000 ) ) ;
#1112=DIRECTION ( 'NONE',  ( 0.000000000000000000, 0.000000000000000000, -1.000000000000000000 ) ) ;
#1116=ORIENTED_EDGE ( 'NONE', *, *, #5437, .F. ) ;
#1155=ORIENTED_EDGE ( 'NONE', *, *, #12032, .T. ) ;
#1181=DIRECTION ( 'NONE',  ( 0.000000000000000000, 0.000000000000000000, -1.000000000000000000 ) ) ;
#1211=DIRECTION ( 'NONE',  ( 0.000000000000000000, 0.000000000000000000, -1.000000000000000000 ) ) ;
#1253=FACE_OUTER_BOUND ( 'NONE', #6147, .T. ) ;
#1281=PLANE ( 'NONE',  #10902 ) ;
#1353=AXIS2_PLACEMENT_3D ( 'NONE', #644, #564, #11000 ) ;
#1354=CIRCLE ( 'NONE', #11881, 0.5000000000000000000 ) ;
#1378=PLANE ( 'NONE',  #2724 ) ;
#1396=EDGE_CURVE ( 'NONE', #8780, #1562, #5587, .T. ) ;
#1422=VERTEX_POINT ( 'NONE', #14761 ) ;
#1444=LINE ( 'NONE', #10494, #3327 ) ;
#1446=ORIENTED_EDGE ( 'NONE', *, *, #3949, .T. ) ;
#1463=DIRECTION ( 'NONE',  ( -0.000000000000000000, -1.000000000000000000, -0.000000000000000000 ) ) ;
#1496=ORIENTED_EDGE ( 'NONE', *, *, #9756, .F. ) ;
#1521=DIRECTION ( 'NONE',  ( 1.000000000000000000, 0.000000000000000000, 0.000000000000000000 ) ) ;
#1542=VECTOR ( 'NONE', #11886, 39.37007874015748143 ) ;
#1550=VECTOR ( 'NONE', #10497, 39.37007874015748143 ) ;
#1562=VERTEX_POINT ( 'NONE', #11552 ) ;
#1599=ADVANCED_FACE ( 'NONE', ( #15147, #6972 ), #8120, .T. ) ;
#1627=DIRECTION ( 'NONE',  ( 1.000000000000000000, 0.000000000000000000, 0.000000000000000000 ) ) ;
#1628=PRODUCT_DEFINITION_SHAPE ( 'NONE', 'NONE',  #3599 ) ;
#1660=ORIENTED_EDGE ( 'NONE', *, *, #5029, .T. ) ;
#1671=ORIENTED_EDGE ( 'NONE', *, *, #12242, .F. ) ;
#1673=LINE ( 'NONE', #7500, #7464 ) ;
#1736=CARTESIAN_POINT ( 'NONE',  ( 0.000000000000000000, 5.750000000000000000, 0.000000000000000000 ) ) ;
#1743=EDGE_CURVE ( 'NONE', #2016, #10545, #8458, .T. ) ;
#1752=PRODUCT ( 'Ball Valve Sub', 'Ball Valve Sub', '', ( #6185 ) ) ;
#1783=VECTOR ( 'NONE', #13825, 39.37007874015748143 ) ;
#1846=ORIENTED_EDGE ( 'NONE', *, *, #10065, .F. ) ;
#1872=DIRECTION ( 'NONE',  ( -0.000000000000000000, -1.000000000000000000, 0.000000000000000000 ) ) ;
#1915=ADVANCED_FACE ( 'NONE', ( #1991 ), #14708, .T. ) ;
#1948=EDGE_LOOP ( 'NONE', ( #4251, #8463, #4769, #134 ) ) ;
#1959=EDGE_CURVE ( 'NONE', #2642, #12259, #3535, .T. ) ;
#1991=FACE_OUTER_BOUND ( 'NONE', #2900, .T. ) ;
#2016=VERTEX_POINT ( 'NONE', #145 ) ;
#2036=VERTEX_POINT ( 'NONE', #12628 ) ;
#2091=SHAPE_REPRESENTATION ( 'Ball Valve Sub', ( #8424 ), #10122 ) ;
#2172=CIRCLE ( 'NONE', #10741, 0.4999999999999997224 ) ;
#2175=AXIS2_PLACEMENT_3D ( 'NONE', #95, #3994, #9312 ) ;
#2237=DIRECTION ( 'NONE',  ( 0.000000000000000000, -1.000000000000000000, 0.000000000000000000 ) ) ;
#2255=DIRECTION ( 'NONE',  ( -0.000000000000000000, -1.000000000000000000, -0.000000000000000000 ) ) ;
#2284=CLOSED_SHELL ( 'NONE', ( #2636, #14870, #10597, #9330, #454, #1599, #325, #2501, #6550, #5036, #6155, #5956, #10561, #1915, #782 ) ) ;
#2287=FACE_OUTER_BOUND ( 'NONE', #10778, .T. ) ;
#2308=DIRECTION ( 'NONE',  ( -0.000000000000000000, -0.000000000000000000, 1.000000000000000000 ) ) ;
#2367=CARTESIAN_POINT ( 'NONE',  ( 0.7500000000000001110, 1.000000000000000000, 0.6614378277661475680 ) ) ;
#2376=ORIENTED_EDGE ( 'NONE', *, *, #12242, .T. ) ;
#2400=VERTEX_POINT ( 'NONE', #4441 ) ;
#2410=VECTOR ( 'NONE', #2308, 39.37007874015748143 ) ;
#2418=EDGE_CURVE ( 'NONE', #14846, #14201, #852, .T. ) ;
#2468=ORIENTED_EDGE ( 'NONE', *, *, #15121, .T. ) ;
#2472=PLANE ( 'NONE',  #12506 ) ;
#2501=ADVANCED_FACE ( 'NONE', ( #2287 ), #1281, .T. ) ;
#2535=DIRECTION ( 'NONE',  ( 0.000000000000000000, -1.000000000000000000, 0.000000000000000000 ) ) ;
#2636=ADVANCED_FACE ( 'NONE', ( #8083 ), #11146, .F. ) ;
#2642=VERTEX_POINT ( 'NONE', #14670 ) ;
#2645=PLANE ( 'NONE',  #11277 ) ;
#2674=PLANE ( 'NONE',  #5719 ) ;
#2702=ORIENTED_EDGE ( 'NONE', *, *, #5994, .T. ) ;
#2724=AXIS2_PLACEMENT_3D ( 'NONE', #10655, #73, #3620 ) ;
#2768=EDGE_LOOP ( 'NONE', ( #1446, #7479, #6384 ) ) ;
#2771=FACE_OUTER_BOUND ( 'NONE', #6150, .T. ) ;
#2777=AXIS2_PLACEMENT_3D ( 'NONE', #8442, #12313, #5369 ) ;
#2782=DIRECTION ( 'NONE',  ( -0.000000000000000000, -1.000000000000000000, -0.000000000000000000 ) ) ;
#2800=ORIENTED_EDGE ( 'NONE', *, *, #8594, .F. ) ;
#2803=EDGE_LOOP ( 'NONE', ( #858, #3536 ) ) ;
#2812=DIRECTION ( 'NONE',  ( -0.000000000000000000, -1.000000000000000000, -0.000000000000000000 ) ) ;
#2813=DIRECTION ( 'NONE',  ( -0.000000000000000000, -0.000000000000000000, 1.000000000000000000 ) ) ;
#2886=EDGE_CURVE ( 'NONE', #8576, #9649, #13059, .T. ) ;
#2900=EDGE_LOOP ( 'NONE', ( #13588, #8380, #1671, #5502 ) ) ;
#2926=ORIENTED_EDGE ( 'NONE', *, *, #3902, .T. ) ;
#2927=CARTESIAN_POINT ( 'NONE',  ( -0.4999999999999996114, 1.866025403784438819, 0.000000000000000000 ) ) ;
#2936=APPLICATION_CONTEXT ( 'automotive_design' ) ;
#2952=VECTOR ( 'NONE', #8098, 39.37007874015748143 ) ;
#2959=LINE ( 'NONE', #13272, #7286 ) ;
#3159=CIRCLE ( 'NONE', #8310, 0.7500000000000001110 ) ;
#3202=ORIENTED_EDGE ( 'NONE', *, *, #14617, .T. ) ;
#3273=ORIENTED_EDGE ( 'NONE', *, *, #15130, .F. ) ;
#3279=ADVANCED_BREP_SHAPE_REPRESENTATION ( '', ( #5275, #8424 ), #10122 ) ;
#3319=CARTESIAN_POINT ( 'NONE',  ( 0.000000000000000000, 4.529999999999999361, 0.000000000000000000 ) ) ;
#3327=VECTOR ( 'NONE', #9579, 39.37007874015748143 ) ;
#3350=AXIS2_PLACEMENT_3D ( 'NONE', #6633, #10224, #12277 ) ;
#3441=LINE ( 'NONE', #13906, #1783 ) ;
#3461=EDGE_CURVE ( 'NONE', #5088, #8576, #1673, .T. ) ;
#3535=LINE ( 'NONE', #11647, #2410 ) ;
#3536=ORIENTED_EDGE ( 'NONE', *, *, #13859, .F. ) ;
#3542=CARTESIAN_POINT ( 'NONE',  ( 0.2849999999999999756, 4.529999999999999361, 0.4108223460329293864 ) ) ;
#3548=EDGE_CURVE ( 'NONE', #14201, #11113, #5762, .T. ) ;
#3598=FACE_OUTER_BOUND ( 'NONE', #2803, .T. ) ;
#3599=PRODUCT_DEFINITION ( 'UNKNOWN', '', #7443, #14727 ) ;
#3620=DIRECTION ( 'NONE',  ( 1.000000000000000000, 0.000000000000000000, 0.000000000000000000 ) ) ;
#3635=DIRECTION ( 'NONE',  ( -1.000000000000000000, 0.000000000000000000, 0.000000000000000000 ) ) ;
#3692=LINE ( 'NONE', #138, #7679 ) ;
#3707=DIRECTION ( 'NONE',  ( -1.000000000000000000, 0.000000000000000000, 0.000000000000000000 ) ) ;
#3845=EDGE_LOOP ( 'NONE', ( #4319, #8287, #5058, #10220, #98, #5618, #9903, #9986, #14760, #3202, #7844, #4895, #6765 ) ) ;
#3878=AXIS2_PLACEMENT_3D ( 'NONE', #10125, #10276, #14934 ) ;
#3902=EDGE_CURVE ( 'NONE', #14857, #909, #12360, .T. ) ;
#3947=LINE ( 'NONE', #13328, #15124 ) ;
#3949=EDGE_CURVE ( 'NONE', #2400, #909, #2959, .T. ) ;
#3960=ORIENTED_EDGE ( 'NONE', *, *, #14017, .T. ) ;
#3962=CARTESIAN_POINT ( 'NONE',  ( -0.7500000000000001110, 1.000000000000000222, -1.000000000000000000 ) ) ;
#3994=DIRECTION ( 'NONE',  ( 0.000000000000000000, -1.000000000000000000, 0.000000000000000000 ) ) ;
#3997=CIRCLE ( 'NONE', #11323, 0.5000000000000000000 ) ;
#4005=AXIS2_PLACEMENT_3D ( 'NONE', #9273, #11718, #9499 ) ;
#4013=DIRECTION ( 'NONE',  ( -1.000000000000000000, 0.000000000000000000, 1.224646799147353207E-16 ) ) ;
#4123=ORIENTED_EDGE ( 'NONE', *, *, #10034, .F. ) ;
#4132=( LENGTH_UNIT ( ) NAMED_UNIT ( * ) SI_UNIT ( $, .METRE. ) );
#4157=ORIENTED_EDGE ( 'NONE', *, *, #14933, .F. ) ;
#4159=DIRECTION ( 'NONE',  ( -3.491481338843132961E-15, 0.000000000000000000, 1.000000000000000000 ) ) ;
#4228=AXIS2_PLACEMENT_3D ( 'NONE', #6216, #14391, #9662 ) ;
#4241=EDGE_LOOP ( 'NONE', ( #12709, #6054 ) ) ;
#4251=ORIENTED_EDGE ( 'NONE', *, *, #885, .F. ) ;
#4263=VERTEX_POINT ( 'NONE', #11157 ) ;
#4319=ORIENTED_EDGE ( 'NONE', *, *, #12895, .T. ) ;
#4354=ORIENTED_EDGE ( 'NONE', *, *, #7650, .F. ) ;
#4362=AXIS2_PLACEMENT_3D ( 'NONE', #10905, #7395, #1627 ) ;
#4371=CARTESIAN_POINT ( 'NONE',  ( 0.000000000000000000, 5.750000000000000000, 0.000000000000000000 ) ) ;
#4441=CARTESIAN_POINT ( 'NONE',  ( -0.2849999999999999756, 4.529999999999999361, -0.4108223460329293864 ) ) ;
#4479=ORIENTED_EDGE ( 'NONE', *, *, #14933, .T. ) ;
#4482=ORIENTED_EDGE ( 'NONE', *, *, #2418, .T. ) ;
#4491=( CONVERSION_BASED_UNIT ( 'INCH', #9086 ) LENGTH_UNIT ( ) NAMED_UNIT ( #11056 ) );
#4524=AXIS2_PLACEMENT_3D ( 'NONE', #1736, #12081, #9865 ) ;
#4525=LINE ( 'NONE', #9197, #1550 ) ;
#4539=AXIS2_PLACEMENT_3D ( 'NONE', #6745, #14766, #904 ) ;
#4543=ORIENTED_EDGE ( 'NONE', *, *, #3949, .F. ) ;
#4599=PLANE ( 'NONE',  #4005 ) ;
#4639=CARTESIAN_POINT ( 'NONE',  ( 0.000000000000000000, 5.750000000000000000, 0.000000000000000000 ) ) ;
#4643=CARTESIAN_POINT ( 'NONE',  ( 6.123233995736762338E-17, 1.866025403784438819, 0.4999999999999995004 ) ) ;
#4769=ORIENTED_EDGE ( 'NONE', *, *, #12691, .F. ) ;
#4771=AXIS2_PLACEMENT_3D ( 'NONE', #7991, #2535, #14946 ) ;
#4779=LINE ( 'NONE', #9602, #13913 ) ;
#4805=AXIS2_PLACEMENT_3D ( 'NONE', #3319, #5393, #5624 ) ;
#4839=EDGE_LOOP ( 'NONE', ( #7972, #7119 ) ) ;
#4870=VERTEX_POINT ( 'NONE', #11289 ) ;
#4877=VECTOR ( 'NONE', #5254, 39.37007874015748143 ) ;
#4884=CARTESIAN_POINT ( 'NONE',  ( -0.2849999999999996425, 0.000000000000000000, -0.4108223460329292753 ) ) ;
#4895=ORIENTED_EDGE ( 'NONE', *, *, #2886, .T. ) ;
#4942=ORIENTED_EDGE ( 'NONE', *, *, #15130, .T. ) ;
#4948=MECHANICAL_DESIGN_GEOMETRIC_PRESENTATION_REPRESENTATION('',(#6158),#6166);
#5029=EDGE_CURVE ( 'NONE', #11113, #10200, #510, .T. ) ;
#5036=ADVANCED_FACE ( 'NONE', ( #9905 ), #2645, .T. ) ;
#5043=ORIENTED_EDGE ( 'NONE', *, *, #5649, .T. ) ;
#5054=CIRCLE ( 'NONE', #7988, 0.4999999999999997224 ) ;
#5058=ORIENTED_EDGE ( 'NONE', *, *, #5994, .F. ) ;
#5062=CARTESIAN_POINT ( 'NONE',  ( 0.000000000000000000, 0.000000000000000000, 0.000000000000000000 ) ) ;
#5088=VERTEX_POINT ( 'NONE', #315 ) ;
#5222=LINE ( 'NONE', #13388, #7570 ) ;
#5237=DIRECTION ( 'NONE',  ( -1.224646799147353207E-16, 0.000000000000000000, -1.000000000000000000 ) ) ;
#5254=DIRECTION ( 'NONE',  ( 0.000000000000000000, -1.000000000000000000, 0.000000000000000000 ) ) ;
#5261=CIRCLE ( 'NONE', #13558, 0.4999999999999997224 ) ;
#5275=MANIFOLD_SOLID_BREP ( 'CirPattern1', #2284 ) ;
#5369=DIRECTION ( 'NONE',  ( 0.000000000000000000, 0.000000000000000000, -1.000000000000000000 ) ) ;
#5393=DIRECTION ( 'NONE',  ( -0.000000000000000000, -1.000000000000000000, 0.000000000000000000 ) ) ;
#5405=UNCERTAINTY_MEASURE_WITH_UNIT (LENGTH_MEASURE( 1.000000000000000082E-05 ), #6729, 'distance_accuracy_value', 'NONE');
#5437=EDGE_CURVE ( 'NONE', #2400, #1562, #1031, .T. ) ;
#5445=ORIENTED_EDGE ( 'NONE', *, *, #1959, .T. ) ;
#5492=FACE_OUTER_BOUND ( 'NONE', #10284, .T. ) ;
#5502=ORIENTED_EDGE ( 'NONE', *, *, #7760, .T. ) ;
#5563=ORIENTED_EDGE ( 'NONE', *, *, #6303, .F. ) ;
#5566=( NAMED_UNIT ( * ) SI_UNIT ( $, .STERADIAN. ) SOLID_ANGLE_UNIT ( ) );
#5569=DIRECTION ( 'NONE',  ( -0.000000000000000000, -1.000000000000000000, -0.000000000000000000 ) ) ;
#5587=CIRCLE ( 'NONE', #6568, 0.5000000000000000000 ) ;
#5618=ORIENTED_EDGE ( 'NONE', *, *, #9134, .T. ) ;
#5624=DIRECTION ( 'NONE',  ( 1.000000000000000000, 0.000000000000000000, 3.491481338843133355E-15 ) ) ;
#5634=VERTEX_POINT ( 'NONE', #3542 ) ;
#5643=CARTESIAN_POINT ( 'NONE',  ( -0.4108223460329260557, 0.000000000000000000, -0.2850000000000041944 ) ) ;
#5649=EDGE_CURVE ( 'NONE', #10545, #14846, #256, .T. ) ;
#5719=AXIS2_PLACEMENT_3D ( 'NONE', #8277, #8355, #200 ) ;
#5762=CIRCLE ( 'NONE', #11626, 0.4999999999999995004 ) ;
#5820=CARTESIAN_POINT ( 'NONE',  ( 0.000000000000000000, 1.866025403784438819, 0.000000000000000000 ) ) ;
#5917=VERTEX_POINT ( 'NONE', #938 ) ;
#5944=AXIS2_PLACEMENT_3D ( 'NONE', #957, #5569, #1112 ) ;
#5956=ADVANCED_FACE ( 'NONE', ( #14879 ), #1378, .T. ) ;
#5962=CIRCLE ( 'NONE', #2777, 0.4999999999999995004 ) ;
#5994=EDGE_CURVE ( 'NONE', #11113, #10545, #5962, .T. ) ;
#6054=ORIENTED_EDGE ( 'NONE', *, *, #14737, .T. ) ;
#6147=EDGE_LOOP ( 'NONE', ( #9432, #8795, #7083 ) ) ;
#6150=EDGE_LOOP ( 'NONE', ( #8089, #1660, #2800, #4482 ) ) ;
#6155=ADVANCED_FACE ( 'NONE', ( #3598 ), #2674, .F. ) ;
#6158=STYLED_ITEM('',(#15206),#5275);
#6166=( GEOMETRIC_REPRESENTATION_CONTEXT ( 3 ) GLOBAL_UNCERTAINTY_ASSIGNED_CONTEXT ( ( #10145 ) ) GLOBAL_UNIT_ASSIGNED_CONTEXT ( ( #4491, #11528, #5566 ) ) REPRESENTATION_CONTEXT ( 'NONE', 'WORKASPACE' ) );
#6168=DIRECTION ( 'NONE',  ( -1.000000000000000000, 0.000000000000000000, -1.047444401652940007E-14 ) ) ;
#6185=PRODUCT_CONTEXT ( 'NONE', #2936, 'mechanical' ) ;
#6195=ORIENTED_EDGE ( 'NONE', *, *, #11829, .F. ) ;
#6216=CARTESIAN_POINT ( 'NONE',  ( 0.000000000000000000, 1.000000000000000000, -0.6614378277661475680 ) ) ;
#6252=AXIS2_PLACEMENT_3D ( 'NONE', #5820, #10485, #12606 ) ;
#6299=SPHERICAL_SURFACE ( 'NONE', #9140, 1.000000000000000000 ) ;
#6303=EDGE_CURVE ( 'NONE', #5917, #2036, #3441, .T. ) ;
#6339=DIRECTION ( 'NONE',  ( 1.000000000000000000, 0.000000000000000000, 0.000000000000000000 ) ) ;
#6377=DIRECTION ( 'NONE',  ( -0.000000000000000000, -0.000000000000000000, -1.000000000000000000 ) ) ;
#6384=ORIENTED_EDGE ( 'NONE', *, *, #14019, .F. ) ;
#6450=CIRCLE ( 'NONE', #8417, 0.7500000000000001110 ) ;
#6550=ADVANCED_FACE ( 'NONE', ( #15149 ), #4599, .F. ) ;
#6555=CIRCLE ( 'NONE', #4362, 0.7500000000000001110 ) ;
#6568=AXIS2_PLACEMENT_3D ( 'NONE', #4371, #7733, #12387 ) ;
#6633=CARTESIAN_POINT ( 'NONE',  ( 0.000000000000000000, 1.000000000000000000, 0.000000000000000000 ) ) ;
#6642=AXIS2_PLACEMENT_3D ( 'NONE', #395, #5237, #4013 ) ;
#6660=CIRCLE ( 'NONE', #4228, 0.7500000000000001110 ) ;
#6668=CARTESIAN_POINT ( 'NONE',  ( 0.2849999999999999756, 4.529999999999999361, 0.4108223460329293864 ) ) ;
#6680=ORIENTED_EDGE ( 'NONE', *, *, #2418, .F. ) ;
#6729=( CONVERSION_BASED_UNIT ( 'INCH', #658 ) LENGTH_UNIT ( ) NAMED_UNIT ( #7450 ) );
#6745=CARTESIAN_POINT ( 'NONE',  ( 0.000000000000000000, 4.529999999999999361, 0.000000000000000000 ) ) ;
#6765=ORIENTED_EDGE ( 'NONE', *, *, #15121, .F. ) ;
#6768=ORIENTED_EDGE ( 'NONE', *, *, #10065, .T. ) ;
#6815=VECTOR ( 'NONE', #1872, 39.37007874015748143 ) ;
#6834=VECTOR ( 'NONE', #2813, 39.37007874015748143 ) ;
#6850=ORIENTED_EDGE ( 'NONE', *, *, #8015, .T. ) ;
#6883=ORIENTED_EDGE ( 'NONE', *, *, #5649, .F. ) ;
#6919=VERTEX_POINT ( 'NONE', #11610 ) ;
#6972=FACE_BOUND ( 'NONE', #4241, .T. ) ;
#6979=VERTEX_POINT ( 'NONE', #10613 ) ;
#7019=CARTESIAN_POINT ( 'NONE',  ( -0.4108223460329263887, 5.750000000000000000, -0.2850000000000042499 ) ) ;
#7083=ORIENTED_EDGE ( 'NONE', *, *, #12895, .F. ) ;
#7105=CARTESIAN_POINT ( 'NONE',  ( 0.000000000000000000, 0.000000000000000000, 0.000000000000000000 ) ) ;
#7119=ORIENTED_EDGE ( 'NONE', *, *, #885, .T. ) ;
#7169=ORIENTED_EDGE ( 'NONE', *, *, #8594, .T. ) ;
#7214=ORIENTED_EDGE ( 'NONE', *, *, #11480, .F. ) ;
#7286=VECTOR ( 'NONE', #6339, 39.37007874015748143 ) ;
#7358=DIRECTION ( 'NONE',  ( 0.000000000000000000, 0.000000000000000000, 1.000000000000000000 ) ) ;
#7395=DIRECTION ( 'NONE',  ( -0.000000000000000000, -0.000000000000000000, 1.000000000000000000 ) ) ;
#7422=ORIENTED_EDGE ( 'NONE', *, *, #9756, .T. ) ;
#7426=PLANE ( 'NONE',  #4524 ) ;
#7443=PRODUCT_DEFINITION_FORMATION_WITH_SPECIFIED_SOURCE ( 'ANY', '', #1752, .NOT_KNOWN. ) ;
#7450=DIMENSIONAL_EXPONENTS ( 1.000000000000000000, 0.000000000000000000, 0.000000000000000000, 0.000000000000000000, 0.000000000000000000, 0.000000000000000000, 0.000000000000000000 ) ;
#7464=VECTOR ( 'NONE', #11888, 39.37007874015748143 ) ;
#7479=ORIENTED_EDGE ( 'NONE', *, *, #9134, .F. ) ;
#7500=CARTESIAN_POINT ( 'NONE',  ( 0.4108223460329293864, 5.750000000000000000, 1.434378554753729569E-15 ) ) ;
#7559=DIRECTION ( 'NONE',  ( 1.000000000000000000, 0.000000000000000000, 0.000000000000000000 ) ) ;
#7570=VECTOR ( 'NONE', #4159, 39.37007874015748143 ) ;
#7641=SHAPE_REPRESENTATION_RELATIONSHIP ( 'NONE' , 'NONE' ,  #2091, #3279 ) ;
#7650=EDGE_CURVE ( 'NONE', #5634, #6979, #12616, .T. ) ;
#7679=VECTOR ( 'NONE', #12620, 39.37007874015748143 ) ;
#7733=DIRECTION ( 'NONE',  ( -0.000000000000000000, -1.000000000000000000, -0.000000000000000000 ) ) ;
#7760=EDGE_CURVE ( 'NONE', #4263, #5088, #1444, .T. ) ;
#7764=CARTESIAN_POINT ( 'NONE',  ( 0.000000000000000000, 4.529999999999999361, 0.000000000000000000 ) ) ;
#7844=ORIENTED_EDGE ( 'NONE', *, *, #11424, .F. ) ;
#7934=( LENGTH_UNIT ( ) NAMED_UNIT ( * ) SI_UNIT ( $, .METRE. ) );
#7972=ORIENTED_EDGE ( 'NONE', *, *, #10034, .T. ) ;
#7988=AXIS2_PLACEMENT_3D ( 'NONE', #8501, #14512, #13144 ) ;
#7991=CARTESIAN_POINT ( 'NONE',  ( 0.000000000000000000, 4.529999999999999361, 0.000000000000000000 ) ) ;
#8015=EDGE_CURVE ( 'NONE', #2016, #6979, #5054, .T. ) ;
#8055=ORIENTED_EDGE ( 'NONE', *, *, #14297, .F. ) ;
#8083=FACE_OUTER_BOUND ( 'NONE', #1948, .T. ) ;
#8089=ORIENTED_EDGE ( 'NONE', *, *, #3548, .T. ) ;
#8098=DIRECTION ( 'NONE',  ( 0.000000000000000000, 1.000000000000000000, 0.000000000000000000 ) ) ;
#8120=SPHERICAL_SURFACE ( 'NONE', #14373, 1.000000000000000000 ) ;
#8149=CARTESIAN_POINT ( 'NONE',  ( -0.4108223460329293864, 5.750000000000000000, -4.303135664261188314E-15 ) ) ;
#8168=FACE_OUTER_BOUND ( 'NONE', #3845, .T. ) ;
#8200=CARTESIAN_POINT ( 'NONE',  ( 0.000000000000000000, 1.000000000000000000, 0.000000000000000000 ) ) ;
#8277=CARTESIAN_POINT ( 'NONE',  ( 0.000000000000000000, 4.529999999999999361, 0.000000000000000000 ) ) ;
#8287=ORIENTED_EDGE ( 'NONE', *, *, #1743, .T. ) ;
#8310=AXIS2_PLACEMENT_3D ( 'NONE', #13496, #8630, #10012 ) ;
#8355=DIRECTION ( 'NONE',  ( 0.000000000000000000, -1.000000000000000000, -0.000000000000000000 ) ) ;
#8380=ORIENTED_EDGE ( 'NONE', *, *, #11424, .T. ) ;
#8417=AXIS2_PLACEMENT_3D ( 'NONE', #12717, #81, #3707 ) ;
#8424=AXIS2_PLACEMENT_3D ( 'NONE', #5062, #7358, #1521 ) ;
#8442=CARTESIAN_POINT ( 'NONE',  ( 0.000000000000000000, 1.866025403784438819, 0.000000000000000000 ) ) ;
#8458=LINE ( 'NONE', #12106, #12419 ) ;
#8462=ORIENTED_EDGE ( 'NONE', *, *, #14666, .F. ) ;
#8463=ORIENTED_EDGE ( 'NONE', *, *, #11480, .T. ) ;
#8501=CARTESIAN_POINT ( 'NONE',  ( 0.000000000000000000, 4.529999999999999361, 0.000000000000000000 ) ) ;
#8538=DIRECTION ( 'NONE',  ( 0.000000000000000000, 0.000000000000000000, -1.000000000000000000 ) ) ;
#8550=DIRECTION ( 'NONE',  ( 1.000000000000000000, 0.000000000000000000, 0.000000000000000000 ) ) ;
#8556=VERTEX_POINT ( 'NONE', #9152 ) ;
#8576=VERTEX_POINT ( 'NONE', #864 ) ;
#8594=EDGE_CURVE ( 'NONE', #14846, #10200, #9952, .T. ) ;
#8596=FACE_BOUND ( 'NONE', #4839, .T. ) ;
#8619=ORIENTED_EDGE ( 'NONE', *, *, #12032, .F. ) ;
#8630=DIRECTION ( 'NONE',  ( 0.000000000000000000, 0.000000000000000000, -1.000000000000000000 ) ) ;
#8656=EDGE_LOOP ( 'NONE', ( #1155, #4942, #4354, #2468 ) ) ;
#8672=AXIS2_PLACEMENT_3D ( 'NONE', #14471, #610, #8538 ) ;
#8693=ORIENTED_EDGE ( 'NONE', *, *, #14666, .T. ) ;
#8750=ORIENTED_EDGE ( 'NONE', *, *, #14019, .T. ) ;
#8780=VERTEX_POINT ( 'NONE', #7019 ) ;
#8795=ORIENTED_EDGE ( 'NONE', *, *, #8015, .F. ) ;
#8817=CARTESIAN_POINT ( 'NONE',  ( 0.000000000000000000, 5.750000000000000000, 0.000000000000000000 ) ) ;
#9086=LENGTH_MEASURE_WITH_UNIT ( LENGTH_MEASURE( 0.02539999999999999897 ), #7934 );
#9112=DIRECTION ( 'NONE',  ( 0.000000000000000000, -1.000000000000000000, 0.000000000000000000 ) ) ;
#9134=EDGE_CURVE ( 'NONE', #8556, #909, #15011, .T. ) ;
#9140=AXIS2_PLACEMENT_3D ( 'NONE', #12178, #6377, #9884 ) ;
#9152=CARTESIAN_POINT ( 'NONE',  ( 0.000000000000000000, 4.529999999999999361, -0.4999999999999997224 ) ) ;
#9176=ORIENTED_EDGE ( 'NONE', *, *, #1743, .F. ) ;
#9197=CARTESIAN_POINT ( 'NONE',  ( -0.2849999999999999201, 0.000000000000000000, 0.4108223460329290533 ) ) ;
#9273=CARTESIAN_POINT ( 'NONE',  ( 0.000000000000000000, 4.529999999999999361, 0.000000000000000000 ) ) ;
#9312=DIRECTION ( 'NONE',  ( -0.000000000000000000, 0.000000000000000000, 1.000000000000000000 ) ) ;
#9330=ADVANCED_FACE ( 'NONE', ( #12231 ), #7426, .F. ) ;
#9345=DIRECTION ( 'NONE',  ( -1.000000000000000000, 0.000000000000000000, 0.000000000000000000 ) ) ;
#9425=LINE ( 'NONE', #14920, #14536 ) ;
#9432=ORIENTED_EDGE ( 'NONE', *, *, #7650, .T. ) ;
#9499=DIRECTION ( 'NONE',  ( 0.000000000000000000, -0.000000000000000000, -1.000000000000000000 ) ) ;
#9579=DIRECTION ( 'NONE',  ( -0.000000000000000000, 1.000000000000000000, -0.000000000000000000 ) ) ;
#9602=CARTESIAN_POINT ( 'NONE',  ( 0.000000000000000000, 5.750000000000000000, 0.4108223460329293864 ) ) ;
#9649=VERTEX_POINT ( 'NONE', #10842 ) ;
#9662=DIRECTION ( 'NONE',  ( 1.000000000000000000, 0.000000000000000000, 0.000000000000000000 ) ) ;
#9672=CYLINDRICAL_SURFACE ( 'NONE', #13883, 0.4999999999999997224 ) ;
#9754=VERTEX_POINT ( 'NONE', #13656 ) ;
#9756=EDGE_CURVE ( 'NONE', #8780, #2036, #10153, .T. ) ;
#9761=CARTESIAN_POINT ( 'NONE',  ( -0.4108223460329322729, 0.000000000000000000, 0.2849999999999953681 ) ) ;
#9865=DIRECTION ( 'NONE',  ( 0.000000000000000000, 0.000000000000000000, -1.000000000000000000 ) ) ;
#9884=DIRECTION ( 'NONE',  ( -1.000000000000000000, 0.000000000000000000, 0.000000000000000000 ) ) ;
#9903=ORIENTED_EDGE ( 'NONE', *, *, #3902, .F. ) ;
#9905=FACE_OUTER_BOUND ( 'NONE', #997, .T. ) ;
#9952=CIRCLE ( 'NONE', #3350, 1.000000000000000000 ) ;
#9958=VECTOR ( 'NONE', #2812, 39.37007874015748143 ) ;
#9986=ORIENTED_EDGE ( 'NONE', *, *, #14297, .T. ) ;
#10012=DIRECTION ( 'NONE',  ( -1.000000000000000000, 0.000000000000000000, 0.000000000000000000 ) ) ;
#10034=EDGE_CURVE ( 'NONE', #2642, #1422, #6555, .T. ) ;
#10065=EDGE_CURVE ( 'NONE', #5917, #9754, #14258, .T. ) ;
#10122=( GEOMETRIC_REPRESENTATION_CONTEXT ( 3 ) GLOBAL_UNCERTAINTY_ASSIGNED_CONTEXT ( ( #5405 ) ) GLOBAL_UNIT_ASSIGNED_CONTEXT ( ( #6729, #807, #735 ) ) REPRESENTATION_CONTEXT ( 'NONE', 'WORKASPACE' ) );
#10125=CARTESIAN_POINT ( 'NONE',  ( 0.4108223460329304411, 5.750000472440944144, -0.2849999999999985323 ) ) ;
#10145=UNCERTAINTY_MEASURE_WITH_UNIT (LENGTH_MEASURE( 1.000000000000000082E-05 ), #4491, 'distance_accuracy_value', 'NONE');
#10150=CIRCLE ( 'NONE', #4539, 0.4999999999999997224 ) ;
#10153=LINE ( 'NONE', #5643, #6815 ) ;
#10200=VERTEX_POINT ( 'NONE', #14237 ) ;
#10220=ORIENTED_EDGE ( 'NONE', *, *, #3548, .F. ) ;
#10224=DIRECTION ( 'NONE',  ( -0.000000000000000000, 0.000000000000000000, 1.000000000000000000 ) ) ;
#10242=ORIENTED_EDGE ( 'NONE', *, *, #3461, .F. ) ;
#10276=DIRECTION ( 'NONE',  ( 1.000000000000000000, 0.000000000000000000, 3.491481338843132961E-15 ) ) ;
#10284=EDGE_LOOP ( 'NONE', ( #7214, #4123, #5445, #13791 ) ) ;
#10400=DIRECTION ( 'NONE',  ( 0.000000000000000000, 0.000000000000000000, -1.000000000000000000 ) ) ;
#10485=DIRECTION ( 'NONE',  ( -0.000000000000000000, -1.000000000000000000, -0.000000000000000000 ) ) ;
#10494=CARTESIAN_POINT ( 'NONE',  ( 0.4108223460329302745, 0.000000000000000000, -0.2849999999999981992 ) ) ;
#10497=DIRECTION ( 'NONE',  ( 0.000000000000000000, -1.000000000000000000, 0.000000000000000000 ) ) ;
#10524=DIRECTION ( 'NONE',  ( 0.000000000000000000, 0.000000000000000000, -1.000000000000000000 ) ) ;
#10545=VERTEX_POINT ( 'NONE', #4643 ) ;
#10561=ADVANCED_FACE ( 'NONE', ( #1253 ), #13308, .F. ) ;
#10578=AXIS2_PLACEMENT_3D ( 'NONE', #13350, #13663, #7559 ) ;
#10597=ADVANCED_FACE ( 'NONE', ( #8168 ), #9672, .T. ) ;
#10613=CARTESIAN_POINT ( 'NONE',  ( -0.2849999999999995315, 4.529999999999999361, 0.4108223460329293864 ) ) ;
#10655=CARTESIAN_POINT ( 'NONE',  ( 0.2849999999999999756, 5.750000472440944144, 0.4108223460329293864 ) ) ;
#10741=AXIS2_PLACEMENT_3D ( 'NONE', #7764, #13480, #12346 ) ;
#10778=EDGE_LOOP ( 'NONE', ( #11694, #2926, #4543, #846 ) ) ;
#10841=SHAPE_DEFINITION_REPRESENTATION ( #1628, #2091 ) ;
#10842=CARTESIAN_POINT ( 'NONE',  ( 0.2849999999999999756, 5.750000000000000000, 0.4108223460329293864 ) ) ;
#10902=AXIS2_PLACEMENT_3D ( 'NONE', #15066, #1211, #13827 ) ;
#10905=CARTESIAN_POINT ( 'NONE',  ( 0.000000000000000000, 1.000000000000000000, -0.6614378277661475680 ) ) ;
#10997=LINE ( 'NONE', #719, #4877 ) ;
#11000=DIRECTION ( 'NONE',  ( 1.000000000000000000, 0.000000000000000000, 0.000000000000000000 ) ) ;
#11056=DIMENSIONAL_EXPONENTS ( 1.000000000000000000, 0.000000000000000000, 0.000000000000000000, 0.000000000000000000, 0.000000000000000000, 0.000000000000000000, 0.000000000000000000 ) ;
#11113=VERTEX_POINT ( 'NONE', #12234 ) ;
#11146=CYLINDRICAL_SURFACE ( 'NONE', #1353, 0.7500000000000001110 ) ;
#11157=CARTESIAN_POINT ( 'NONE',  ( 0.4108223460329304411, 4.529999999999999361, -0.2849999999999985323 ) ) ;
#11277=AXIS2_PLACEMENT_3D ( 'NONE', #14257, #6168, #12120 ) ;
#11289=CARTESIAN_POINT ( 'NONE',  ( -0.2849999999999999756, 5.750000000000000000, 0.4108223460329293864 ) ) ;
#11323=AXIS2_PLACEMENT_3D ( 'NONE', #8817, #11408, #13759 ) ;
#11408=DIRECTION ( 'NONE',  ( -0.000000000000000000, -1.000000000000000000, -0.000000000000000000 ) ) ;
#11424=EDGE_CURVE ( 'NONE', #8576, #6919, #10997, .T. ) ;
#11480=EDGE_CURVE ( 'NONE', #1422, #14862, #640, .T. ) ;
#11486=DIRECTION ( 'NONE',  ( -1.000000000000000000, 0.000000000000000000, 0.000000000000000000 ) ) ;
#11528=( NAMED_UNIT ( * ) PLANE_ANGLE_UNIT ( ) SI_UNIT ( $, .RADIAN. ) );
#11536=APPLICATION_CONTEXT ( 'automotive_design' ) ;
#11552=CARTESIAN_POINT ( 'NONE',  ( -0.2849999999999999756, 5.750000000000000000, -0.4108223460329293864 ) ) ;
#11556=DIRECTION ( 'NONE',  ( 0.000000000000000000, 0.000000000000000000, -1.000000000000000000 ) ) ;
#11610=CARTESIAN_POINT ( 'NONE',  ( 0.4108223460329283871, 4.529999999999999361, 0.2850000000000009748 ) ) ;
#11626=AXIS2_PLACEMENT_3D ( 'NONE', #14755, #970, #10400 ) ;
#11647=CARTESIAN_POINT ( 'NONE',  ( 0.7500000000000001110, 1.000000000000000000, -1.000000000000000000 ) ) ;
#11694=ORIENTED_EDGE ( 'NONE', *, *, #11829, .T. ) ;
#11718=DIRECTION ( 'NONE',  ( 0.000000000000000000, -1.000000000000000000, 0.000000000000000000 ) ) ;
#11803=DIRECTION ( 'NONE',  ( 1.000000000000000000, 0.000000000000000000, 3.491481338843132961E-15 ) ) ;
#11809=LINE ( 'NONE', #8149, #1542 ) ;
#11829=EDGE_CURVE ( 'NONE', #1562, #14857, #3947, .T. ) ;
#11878=CARTESIAN_POINT ( 'NONE',  ( 0.000000000000000000, 4.529999999999999361, 0.000000000000000000 ) ) ;
#11881=AXIS2_PLACEMENT_3D ( 'NONE', #4639, #2255, #10524 ) ;
#11886=DIRECTION ( 'NONE',  ( 1.047444401652940007E-14, 0.000000000000000000, -1.000000000000000000 ) ) ;
#11888=DIRECTION ( 'NONE',  ( -3.491481338843132961E-15, 0.000000000000000000, 1.000000000000000000 ) ) ;
#12032=EDGE_CURVE ( 'NONE', #9649, #4870, #4779, .T. ) ;
#12081=DIRECTION ( 'NONE',  ( 0.000000000000000000, -1.000000000000000000, -0.000000000000000000 ) ) ;
#12106=CARTESIAN_POINT ( 'NONE',  ( 6.123233995736763571E-17, 0.000000000000000000, 0.4999999999999997224 ) ) ;
#12120=DIRECTION ( 'NONE',  ( -1.047444401652940007E-14, 0.000000000000000000, 1.000000000000000000 ) ) ;
#12133=EDGE_LOOP ( 'NONE', ( #14663, #2702, #5043, #7169 ) ) ;
#12178=CARTESIAN_POINT ( 'NONE',  ( 0.000000000000000000, 1.000000000000000000, 0.000000000000000000 ) ) ;
#12231=FACE_OUTER_BOUND ( 'NONE', #1036, .T. ) ;
#12234=CARTESIAN_POINT ( 'NONE',  ( 0.4999999999999996114, 1.866025403784438819, -6.123233995736761105E-17 ) ) ;
#12242=EDGE_CURVE ( 'NONE', #4263, #6919, #5222, .T. ) ;
#12259=VERTEX_POINT ( 'NONE', #2367 ) ;
#12277=DIRECTION ( 'NONE',  ( 1.000000000000000000, 0.000000000000000000, 0.000000000000000000 ) ) ;
#12313=DIRECTION ( 'NONE',  ( -0.000000000000000000, -1.000000000000000000, -0.000000000000000000 ) ) ;
#12346=DIRECTION ( 'NONE',  ( 0.000000000000000000, 0.000000000000000000, 1.000000000000000000 ) ) ;
#12360=LINE ( 'NONE', #639, #9958 ) ;
#12387=DIRECTION ( 'NONE',  ( 0.000000000000000000, 0.000000000000000000, -1.000000000000000000 ) ) ;
#12419=VECTOR ( 'NONE', #2782, 39.37007874015748143 ) ;
#12476=AXIS2_PLACEMENT_3D ( 'NONE', #12946, #1463, #13090 ) ;
#12494=ORIENTED_EDGE ( 'NONE', *, *, #14617, .F. ) ;
#12506=AXIS2_PLACEMENT_3D ( 'NONE', #11878, #2237, #11803 ) ;
#12590=ORIENTED_EDGE ( 'NONE', *, *, #13859, .T. ) ;
#12606=DIRECTION ( 'NONE',  ( 0.000000000000000000, 0.000000000000000000, -1.000000000000000000 ) ) ;
#12616=LINE ( 'NONE', #6668, #14558 ) ;
#12620=DIRECTION ( 'NONE',  ( -0.000000000000000000, 1.000000000000000000, -0.000000000000000000 ) ) ;
#12628=CARTESIAN_POINT ( 'NONE',  ( -0.4108223460329263887, 4.529999999999999361, -0.2850000000000038058 ) ) ;
#12691=EDGE_CURVE ( 'NONE', #12259, #14862, #3159, .T. ) ;
#12709=ORIENTED_EDGE ( 'NONE', *, *, #12691, .T. ) ;
#12717=CARTESIAN_POINT ( 'NONE',  ( 0.000000000000000000, 1.000000000000000000, 0.6614378277661475680 ) ) ;
#12817=CYLINDRICAL_SURFACE ( 'NONE', #5944, 0.4999999999999997224 ) ;
#12895=EDGE_CURVE ( 'NONE', #5634, #2016, #2172, .T. ) ;
#12945=ORIENTED_EDGE ( 'NONE', *, *, #2886, .F. ) ;
#12946=CARTESIAN_POINT ( 'NONE',  ( 0.000000000000000000, 1.866025403784438819, 0.000000000000000000 ) ) ;
#13010=FACE_OUTER_BOUND ( 'NONE', #13507, .T. ) ;
#13059=CIRCLE ( 'NONE', #8672, 0.5000000000000000000 ) ;
#13090=DIRECTION ( 'NONE',  ( 0.000000000000000000, 0.000000000000000000, -1.000000000000000000 ) ) ;
#13094=CARTESIAN_POINT ( 'NONE',  ( 0.2849999999999999756, 5.750000000000000000, -0.4108223460329293864 ) ) ;
#13144=DIRECTION ( 'NONE',  ( 0.000000000000000000, 0.000000000000000000, 1.000000000000000000 ) ) ;
#13161=CARTESIAN_POINT ( 'NONE',  ( 0.2849999999999998090, 4.529999999999999361, -0.4108223460329292198 ) ) ;
#13232=CARTESIAN_POINT ( 'NONE',  ( -0.7500000000000001110, 1.000000000000000222, 0.6614378277661475680 ) ) ;
#13272=CARTESIAN_POINT ( 'NONE',  ( -0.2849999999999999756, 4.529999999999999361, -0.4108223460329293864 ) ) ;
#13308=PLANE ( 'NONE',  #2175 ) ;
#13328=CARTESIAN_POINT ( 'NONE',  ( 0.000000000000000000, 5.750000000000000000, -0.4108223460329293864 ) ) ;
#13350=CARTESIAN_POINT ( 'NONE',  ( 0.000000000000000000, 1.000000000000000000, -1.000000000000000000 ) ) ;
#13388=CARTESIAN_POINT ( 'NONE',  ( 0.4108223460329304411, 4.529999999999999361, -0.2849999999999985323 ) ) ;
#13480=DIRECTION ( 'NONE',  ( 0.000000000000000000, -1.000000000000000000, 0.000000000000000000 ) ) ;
#13496=CARTESIAN_POINT ( 'NONE',  ( 0.000000000000000000, 1.000000000000000000, 0.6614378277661475680 ) ) ;
#13507=EDGE_LOOP ( 'NONE', ( #2376, #12494 ) ) ;
#13558=AXIS2_PLACEMENT_3D ( 'NONE', #1059, #9112, #11556 ) ;
#13588=ORIENTED_EDGE ( 'NONE', *, *, #3461, .T. ) ;
#13656=CARTESIAN_POINT ( 'NONE',  ( -0.4108223460329323840, 5.750000000000000000, 0.2849999999999956457 ) ) ;
#13663=DIRECTION ( 'NONE',  ( -0.000000000000000000, -0.000000000000000000, 1.000000000000000000 ) ) ;
#13759=DIRECTION ( 'NONE',  ( 0.000000000000000000, 0.000000000000000000, -1.000000000000000000 ) ) ;
#13791=ORIENTED_EDGE ( 'NONE', *, *, #14737, .F. ) ;
#13793=CARTESIAN_POINT ( 'NONE',  ( 0.000000000000000000, 1.866025403784438819, -0.4999999999999995004 ) ) ;
#13825=DIRECTION ( 'NONE',  ( 1.047444401652940007E-14, 0.000000000000000000, -1.000000000000000000 ) ) ;
#13827=DIRECTION ( 'NONE',  ( -1.000000000000000000, 0.000000000000000000, -0.000000000000000000 ) ) ;
#13859=EDGE_CURVE ( 'NONE', #5917, #2036, #10150, .T. ) ;
#13883=AXIS2_PLACEMENT_3D ( 'NONE', #7105, #14029, #1181 ) ;
#13906=CARTESIAN_POINT ( 'NONE',  ( -0.4108223460329323840, 4.529999999999999361, 0.2849999999999956457 ) ) ;
#13909=DIRECTION ( 'NONE',  ( -0.000000000000000000, -0.000000000000000000, -1.000000000000000000 ) ) ;
#13913=VECTOR ( 'NONE', #3635, 39.37007874015748143 ) ;
#14012=ORIENTED_EDGE ( 'NONE', *, *, #1396, .T. ) ;
#14017=EDGE_CURVE ( 'NONE', #8556, #14201, #9425, .T. ) ;
#14019=EDGE_CURVE ( 'NONE', #2400, #8556, #5261, .T. ) ;
#14029=DIRECTION ( 'NONE',  ( -0.000000000000000000, -1.000000000000000000, -0.000000000000000000 ) ) ;
#14039=FACE_OUTER_BOUND ( 'NONE', #14826, .T. ) ;
#14066=DIRECTION ( 'NONE',  ( -0.000000000000000000, -1.000000000000000000, -0.000000000000000000 ) ) ;
#14201=VERTEX_POINT ( 'NONE', #13793 ) ;
#14237=CARTESIAN_POINT ( 'NONE',  ( -6.123233995736766036E-17, 0.000000000000000000, 0.000000000000000000 ) ) ;
#14257=CARTESIAN_POINT ( 'NONE',  ( -0.4108223460329323840, 5.750000472440944144, 0.2849999999999956457 ) ) ;
#14258=LINE ( 'NONE', #9761, #14858 ) ;
#14297=EDGE_CURVE ( 'NONE', #14857, #5088, #1354, .T. ) ;
#14373=AXIS2_PLACEMENT_3D ( 'NONE', #8200, #13909, #9345 ) ;
#14391=DIRECTION ( 'NONE',  ( -0.000000000000000000, -0.000000000000000000, 1.000000000000000000 ) ) ;
#14471=CARTESIAN_POINT ( 'NONE',  ( 0.000000000000000000, 5.750000000000000000, 0.000000000000000000 ) ) ;
#14488=ORIENTED_EDGE ( 'NONE', *, *, #1396, .F. ) ;
#14512=DIRECTION ( 'NONE',  ( 0.000000000000000000, -1.000000000000000000, 0.000000000000000000 ) ) ;
#14536=VECTOR ( 'NONE', #14066, 39.37007874015748143 ) ;
#14558=VECTOR ( 'NONE', #11486, 39.37007874015748143 ) ;
#14617=EDGE_CURVE ( 'NONE', #4263, #6919, #861, .T. ) ;
#14663=ORIENTED_EDGE ( 'NONE', *, *, #5029, .F. ) ;
#14666=EDGE_CURVE ( 'NONE', #9754, #8780, #11809, .T. ) ;
#14670=CARTESIAN_POINT ( 'NONE',  ( 0.7500000000000001110, 1.000000000000000000, -0.6614378277661475680 ) ) ;
#14708=PLANE ( 'NONE',  #3878 ) ;
#14727=PRODUCT_DEFINITION_CONTEXT ( 'detailed design', #11536, 'design' ) ;
#14737=EDGE_CURVE ( 'NONE', #14862, #12259, #6450, .T. ) ;
#14755=CARTESIAN_POINT ( 'NONE',  ( 0.000000000000000000, 1.866025403784438819, 0.000000000000000000 ) ) ;
#14760=ORIENTED_EDGE ( 'NONE', *, *, #7760, .F. ) ;
#14761=CARTESIAN_POINT ( 'NONE',  ( -0.7500000000000001110, 1.000000000000000222, -0.6614378277661475680 ) ) ;
#14766=DIRECTION ( 'NONE',  ( 0.000000000000000000, -1.000000000000000000, 0.000000000000000000 ) ) ;
#14826=EDGE_LOOP ( 'NONE', ( #9176, #6850, #3273, #4479, #1846, #12590, #1496, #14012, #1116, #8750, #3960, #6680, #6883 ) ) ;
#14846=VERTEX_POINT ( 'NONE', #2927 ) ;
#14857=VERTEX_POINT ( 'NONE', #13094 ) ;
#14858=VECTOR ( 'NONE', #250, 39.37007874015748143 ) ;
#14862=VERTEX_POINT ( 'NONE', #13232 ) ;
#14870=ADVANCED_FACE ( 'NONE', ( #8596, #2771 ), #6299, .T. ) ;
#14879=FACE_OUTER_BOUND ( 'NONE', #8656, .T. ) ;
#14920=CARTESIAN_POINT ( 'NONE',  ( 0.000000000000000000, 0.000000000000000000, -0.4999999999999997224 ) ) ;
#14933=EDGE_CURVE ( 'NONE', #4870, #9754, #3997, .T. ) ;
#14934=DIRECTION ( 'NONE',  ( 3.491481338843132961E-15, 0.000000000000000000, -1.000000000000000000 ) ) ;
#14946=DIRECTION ( 'NONE',  ( 0.000000000000000000, 0.000000000000000000, -1.000000000000000000 ) ) ;
#15011=CIRCLE ( 'NONE', #4771, 0.4999999999999997224 ) ;
#15066=CARTESIAN_POINT ( 'NONE',  ( -0.2849999999999999756, 5.750000472440944144, -0.4108223460329293864 ) ) ;
#15121=EDGE_CURVE ( 'NONE', #5634, #9649, #3692, .T. ) ;
#15124=VECTOR ( 'NONE', #8550, 39.37007874015748143 ) ;
#15130=EDGE_CURVE ( 'NONE', #4870, #6979, #4525, .T. ) ;
#15147=FACE_OUTER_BOUND ( 'NONE', #12133, .T. ) ;
#15149=FACE_OUTER_BOUND ( 'NONE', #2768, .T. ) ;
#15200=COLOUR_RGB('Off White',0.89,0.88,0.83);
#15201=FILL_AREA_STYLE_COLOUR('',#15200);
#15202=FILL_AREA_STYLE('',(#15201));
#15203=SURFACE_STYLE_FILL_AREA(#15202);
#15204=SURFACE_SIDE_STYLE('',(#15203));
#15205=SURFACE_STYLE_USAGE(.BOTH.,#15204);
#15206=PRESENTATION_STYLE_ASSIGNMENT((#15205));
ENDSEC;
END-ISO-10303-21;
